ISO-10303-21;
HEADER;
FILE_DESCRIPTION (('STEP AP214'),
    '1' );
FILE_NAME ('socket head cap screw_iso_ISO 4762 M12 x 80 - 36N.step',
    '2026-10-19T17:36:30',
    ( '' ),
    ( '' ),
    'SwSTEP 2.0',
    'SolidWorks 2025',
    '' );
FILE_SCHEMA (( 'AUTOMOTIVE_DESIGN' ));
ENDSEC;

DATA;
#39=DIRECTION ( 'NONE',  ( 0.000000000000000000, -1.000000000000000000, 1.039664082171044875E-15 ) ) ;
#46=ORIENTED_EDGE ( 'NONE', *, *, #5665, .T. ) ;
#60=EDGE_CURVE ( 'NONE', #174, #10109, #7975, .T. ) ;
#71=ORIENTED_EDGE ( 'NONE', *, *, #4541, .F. ) ;
#98=VECTOR ( 'NONE', #4798, 1000.000000000000000 ) ;
#105=FACE_OUTER_BOUND ( 'NONE', #3848, .T. ) ;
#117=PRODUCT_DEFINITION_SHAPE ( 'NONE', 'NONE',  #10531 ) ;
#174=VERTEX_POINT ( 'NONE', #10304 ) ;
#178=LINE ( 'NONE', #1320, #6017 ) ;
#190=( GEOMETRIC_REPRESENTATION_CONTEXT ( 3 ) GLOBAL_UNCERTAINTY_ASSIGNED_CONTEXT ( ( #2001 ) ) GLOBAL_UNIT_ASSIGNED_CONTEXT ( ( #12461, #11571, #6744 ) ) REPRESENTATION_CONTEXT ( 'NONE', 'WORKASPACE' ) );
#202=DIRECTION ( 'NONE',  ( -1.000000000000000000, -0.000000000000000000, -0.000000000000000000 ) ) ;
#207=DIRECTION ( 'NONE',  ( 1.000000000000000000, 0.000000000000000000, 0.000000000000000000 ) ) ;
#268=ORIENTED_EDGE ( 'NONE', *, *, #60, .F. ) ;
#282=ORIENTED_EDGE ( 'NONE', *, *, #2101, .F. ) ;
#286=DIRECTION ( 'NONE',  ( -1.000000000000000000, -0.000000000000000000, -0.000000000000000000 ) ) ;
#306=CARTESIAN_POINT ( 'NONE',  ( 12.00000000000000000, 8.082668874372530033E-16, 6.599999999999998757 ) ) ;
#334=CARTESIAN_POINT ( 'NONE',  ( 92.00000000000000000, 0.000000000000000000, 0.000000000000000000 ) ) ;
#339=VECTOR ( 'NONE', #6071, 1000.000000000000000 ) ;
#370=FACE_OUTER_BOUND ( 'NONE', #7720, .T. ) ;
#379=VECTOR ( 'NONE', #39, 1000.000000000000000 ) ;
#393=ORIENTED_EDGE ( 'NONE', *, *, #1641, .T. ) ;
#406=CARTESIAN_POINT ( 'NONE',  ( 0.000000000000000000, 2.919948986426526005, -5.057500000000003659 ) ) ;
#408=DIRECTION ( 'NONE',  ( -1.000000000000000000, 0.000000000000000000, 0.000000000000000000 ) ) ;
#409=VERTEX_POINT ( 'NONE', #1238 ) ;
#438=VERTEX_POINT ( 'NONE', #3133 ) ;
#448=CARTESIAN_POINT ( 'NONE',  ( 6.000000000000000000, 5.839897972853064445, -8.673617379884035472E-15 ) ) ;
#470=DIRECTION ( 'NONE',  ( -1.000000000000000000, -0.000000000000000000, -0.000000000000000000 ) ) ;
#486=DIRECTION ( 'NONE',  ( -1.000000000000000000, -0.000000000000000000, -0.000000000000000000 ) ) ;
#488=CARTESIAN_POINT ( 'NONE',  ( 6.000000000000000000, 5.839897972853064445, -8.673617379884035472E-15 ) ) ;
#491=DIRECTION ( 'NONE',  ( 0.000000000000000000, 0.000000000000000000, 1.000000000000000000 ) ) ;
#497=DIRECTION ( 'NONE',  ( 0.000000000000000000, 0.000000000000000000, -1.000000000000000000 ) ) ;
#516=DIRECTION ( 'NONE',  ( 0.000000000000000000, 0.000000000000000000, -1.000000000000000000 ) ) ;
#518=ORIENTED_EDGE ( 'NONE', *, *, #11469, .T. ) ;
#560=CARTESIAN_POINT ( 'NONE',  ( 6.000000000000000000, -5.839897972853060892, 7.806255641895631925E-15 ) ) ;
#590=AXIS2_PLACEMENT_3D ( 'NONE', #448, #12242, #3603 ) ;
#619=CARTESIAN_POINT ( 'NONE',  ( 12.59999999999999964, 0.000000000000000000, 0.000000000000000000 ) ) ;
#623=EDGE_LOOP ( 'NONE', ( #2309, #2368, #2131 ) ) ;
#637=VERTEX_POINT ( 'NONE', #5729 ) ;
#657=CYLINDRICAL_SURFACE ( 'NONE', #974, 5.999999999999999112 ) ;
#676=DIRECTION ( 'NONE',  ( 0.000000000000000000, 0.000000000000000000, 1.000000000000000000 ) ) ;
#684=CARTESIAN_POINT ( 'NONE',  ( 12.59999999999999964, 0.000000000000000000, 5.999999999999999112 ) ) ;
#695=ORIENTED_EDGE ( 'NONE', *, *, #9724, .T. ) ;
#697=EDGE_CURVE ( 'NONE', #1603, #438, #5063, .T. ) ;
#733=CARTESIAN_POINT ( 'NONE',  ( 6.000000000000000000, 0.000000000000000000, 5.057500000000000107 ) ) ;
#743=ORIENTED_EDGE ( 'NONE', *, *, #1458, .F. ) ;
#752=LINE ( 'NONE', #10574, #10296 ) ;
#773=EDGE_LOOP ( 'NONE', ( #9656, #898, #9194, #268, #11639 ) ) ;
#776=DIRECTION ( 'NONE',  ( -1.000000000000000000, -0.000000000000000000, -0.000000000000000000 ) ) ;
#791=EDGE_CURVE ( 'NONE', #2265, #6417, #2144, .T. ) ;
#810=FACE_OUTER_BOUND ( 'NONE', #773, .T. ) ;
#817=ORIENTED_EDGE ( 'NONE', *, *, #10768, .T. ) ;
#819=PLANE ( 'NONE',  #5906 ) ;
#845=CARTESIAN_POINT ( 'NONE',  ( 6.000000000000000000, 2.919948986426526005, -5.057500000000003659 ) ) ;
#846=DIRECTION ( 'NONE',  ( 0.000000000000000000, -1.039664082171044875E-15, -1.000000000000000000 ) ) ;
#864=ORIENTED_EDGE ( 'NONE', *, *, #2205, .T. ) ;
#888=PRODUCT_DEFINITION_FORMATION_WITH_SPECIFIED_SOURCE ( 'ANY', '', #2946, .NOT_KNOWN. ) ;
#898=ORIENTED_EDGE ( 'NONE', *, *, #12369, .F. ) ;
#899=VECTOR ( 'NONE', #7447, 1000.000000000000114 ) ;
#901=EDGE_LOOP ( 'NONE', ( #6804, #8146, #864, #518, #4487 ) ) ;
#907=CARTESIAN_POINT ( 'NONE',  ( 91.03600000000000136, 0.000000000000000000, 0.000000000000000000 ) ) ;
#938=VERTEX_POINT ( 'NONE', #4530 ) ;
#974=AXIS2_PLACEMENT_3D ( 'NONE', #12267, #776, #3567 ) ;
#989=AXIS2_PLACEMENT_3D ( 'NONE', #9387, #11468, #6581 ) ;
#995=AXIS2_PLACEMENT_3D ( 'NONE', #11324, #486, #3395 ) ;
#1065=ORIENTED_EDGE ( 'NONE', *, *, #2468, .F. ) ;
#1066=EDGE_LOOP ( 'NONE', ( #393, #7519, #11014, #6682 ) ) ;
#1092=CARTESIAN_POINT ( 'NONE',  ( 6.000000000000000000, 5.839897972853064445, -8.673617379884035472E-15 ) ) ;
#1096=( GEOMETRIC_REPRESENTATION_CONTEXT ( 3 ) GLOBAL_UNCERTAINTY_ASSIGNED_CONTEXT ( ( #6777 ) ) GLOBAL_UNIT_ASSIGNED_CONTEXT ( ( #2294, #11170, #6348 ) ) REPRESENTATION_CONTEXT ( 'NONE', 'WORKASPACE' ) );
#1113=ADVANCED_FACE ( 'NONE', ( #9378 ), #5191, .F. ) ;
#1116=DIRECTION ( 'NONE',  ( -1.000000000000000000, -0.000000000000000000, -0.000000000000000000 ) ) ;
#1172=CARTESIAN_POINT ( 'NONE',  ( 12.59999999999999964, 7.347880794884118750E-16, -5.999999999999999112 ) ) ;
#1196=EDGE_CURVE ( 'NONE', #6710, #2612, #4774, .T. ) ;
#1224=DIRECTION ( 'NONE',  ( 0.000000000000000000, 0.000000000000000000, 1.000000000000000000 ) ) ;
#1238=CARTESIAN_POINT ( 'NONE',  ( 6.000000000000000000, -4.379923479639802331, -2.528749999999991616 ) ) ;
#1244=FACE_OUTER_BOUND ( 'NONE', #7078, .T. ) ;
#1292=VERTEX_POINT ( 'NONE', #11460 ) ;
#1320=CARTESIAN_POINT ( 'NONE',  ( 0.000000000000000000, -2.919948986426523341, 5.057500000000002771 ) ) ;
#1321=ADVANCED_FACE ( 'NONE', ( #10437, #3845 ), #12353, .T. ) ;
#1343=ORIENTED_EDGE ( 'NONE', *, *, #11108, .T. ) ;
#1377=LINE ( 'NONE', #11841, #2958 ) ;
#1427=CYLINDRICAL_SURFACE ( 'NONE', #10025, 9.000000000000000000 ) ;
#1442=AXIS2_PLACEMENT_3D ( 'NONE', #2014, #7796, #2975 ) ;
#1445=FACE_OUTER_BOUND ( 'NONE', #2596, .T. ) ;
#1454=ORIENTED_EDGE ( 'NONE', *, *, #8944, .F. ) ;
#1457=DIRECTION ( 'NONE',  ( 0.000000000000000000, 0.000000000000000000, 1.000000000000000000 ) ) ;
#1458=EDGE_CURVE ( 'NONE', #7136, #637, #1377, .T. ) ;
#1467=CARTESIAN_POINT ( 'NONE',  ( 12.59999999999999964, 0.000000000000000000, -6.599999999999998757 ) ) ;
#1483=CARTESIAN_POINT ( 'NONE',  ( -31.74999999999995737, 0.000000000000000000, 0.000000000000000000 ) ) ;
#1528=SHAPE_REPRESENTATION_RELATIONSHIP ( 'NONE' , 'NONE' ,  #10815, #4292 ) ;
#1529=AXIS2_PLACEMENT_3D ( 'NONE', #7516, #10550, #10487 ) ;
#1561=CARTESIAN_POINT ( 'NONE',  ( 12.00000000000000355, 0.000000000000000000, 0.000000000000000000 ) ) ;
#1575=EDGE_CURVE ( 'NONE', #9559, #11430, #8792, .T. ) ;
#1603=VERTEX_POINT ( 'NONE', #10751 ) ;
#1608=CARTESIAN_POINT ( 'NONE',  ( 0.000000000000000000, 5.839897972853064445, -8.673617379884035472E-15 ) ) ;
#1641=EDGE_CURVE ( 'NONE', #1292, #7797, #6003, .T. ) ;
#1647=ORIENTED_EDGE ( 'NONE', *, *, #1575, .F. ) ;
#1648=CARTESIAN_POINT ( 'NONE',  ( 6.000000000000000000, -2.919948986426523341, 5.057500000000002771 ) ) ;
#1681=VECTOR ( 'NONE', #2476, 1000.000000000000000 ) ;
#1734=ORIENTED_EDGE ( 'NONE', *, *, #2101, .T. ) ;
#1773=ORIENTED_EDGE ( 'NONE', *, *, #12369, .T. ) ;
#1774=EDGE_CURVE ( 'NONE', #11133, #10329, #7061, .T. ) ;
#1825=ORIENTED_EDGE ( 'NONE', *, *, #1954, .T. ) ;
#1830=MANIFOLD_SOLID_BREP ( 'Hex', #2005 ) ;
#1844=ORIENTED_EDGE ( 'NONE', *, *, #8243, .F. ) ;
#1871=ADVANCED_FACE ( 'NONE', ( #4061 ), #5020, .T. ) ;
#1892=VECTOR ( 'NONE', #5489, 999.9999999999998863 ) ;
#1909=CARTESIAN_POINT ( 'NONE',  ( 6.000000000000000000, 5.839897972853064445, -8.673617379884035472E-15 ) ) ;
#1934=LINE ( 'NONE', #6508, #6749 ) ;
#1946=DIRECTION ( 'NONE',  ( 0.000000000000000000, 0.000000000000000000, 1.000000000000000000 ) ) ;
#1954=EDGE_CURVE ( 'NONE', #938, #637, #2198, .T. ) ;
#1987=ADVANCED_FACE ( 'NONE', ( #4925, #3903 ), #6823, .T. ) ;
#1989=AXIS2_PLACEMENT_3D ( 'NONE', #5639, #4746, #9512 ) ;
#2001=UNCERTAINTY_MEASURE_WITH_UNIT (LENGTH_MEASURE( 1.000000000000000082E-05 ), #12461, 'distance_accuracy_value', 'NONE');
#2005=CLOSED_SHELL ( 'NONE', ( #2536, #9645, #12084, #12329, #9249, #8671, #1321, #5617, #4519, #10116, #1987, #7678, #1113, #5280, #6311, #3115, #1871, #5075, #4886, #10073, #4577, #2570, #9477, #3656, #3912, #4181, #11801 ) ) ;
#2014=CARTESIAN_POINT ( 'NONE',  ( 92.00000000000000000, 0.000000000000000000, 0.000000000000000000 ) ) ;
#2018=EDGE_CURVE ( 'NONE', #7797, #1292, #5646, .T. ) ;
#2043=DIRECTION ( 'NONE',  ( 0.000000000000000000, -0.4999999999999983902, 0.8660254037844395958 ) ) ;
#2046=LINE ( 'NONE', #2111, #12359 ) ;
#2049=EDGE_LOOP ( 'NONE', ( #5398, #4959, #5054, #8702, #10093 ) ) ;
#2058=ORIENTED_EDGE ( 'NONE', *, *, #7609, .F. ) ;
#2076=DIRECTION ( 'NONE',  ( 0.000000000000000000, -1.000000000000000000, 1.039664082171044875E-15 ) ) ;
#2094=ORIENTED_EDGE ( 'NONE', *, *, #9469, .F. ) ;
#2097=DIRECTION ( 'NONE',  ( -1.000000000000000000, -0.000000000000000000, -0.000000000000000000 ) ) ;
#2101=EDGE_CURVE ( 'NONE', #9553, #5036, #11989, .T. ) ;
#2111=CARTESIAN_POINT ( 'NONE',  ( 6.000000000000000000, -2.919948986426523341, 5.057500000000002771 ) ) ;
#2123=CARTESIAN_POINT ( 'NONE',  ( 0.000000000000000000, 2.919948986426526005, -5.057500000000003659 ) ) ;
#2127=DIRECTION ( 'NONE',  ( 1.000000000000000000, 0.000000000000000000, 0.000000000000000000 ) ) ;
#2131=ORIENTED_EDGE ( 'NONE', *, *, #6444, .T. ) ;
#2144=CIRCLE ( 'NONE', #6394, 5.035999999999999588 ) ;
#2161=FACE_OUTER_BOUND ( 'NONE', #5184, .T. ) ;
#2174=EDGE_CURVE ( 'NONE', #5616, #409, #4144, .T. ) ;
#2198=LINE ( 'NONE', #7074, #12270 ) ;
#2205=EDGE_CURVE ( 'NONE', #4253, #7687, #2046, .T. ) ;
#2231=EDGE_CURVE ( 'NONE', #1292, #2612, #7764, .T. ) ;
#2265=VERTEX_POINT ( 'NONE', #3376 ) ;
#2288=ORIENTED_EDGE ( 'NONE', *, *, #7234, .T. ) ;
#2294=( LENGTH_UNIT ( ) NAMED_UNIT ( * ) SI_UNIT ( .MILLI., .METRE. ) );
#2307=VERTEX_POINT ( 'NONE', #406 ) ;
#2309=ORIENTED_EDGE ( 'NONE', *, *, #7493, .F. ) ;
#2354=VERTEX_POINT ( 'NONE', #8145 ) ;
#2367=VECTOR ( 'NONE', #2399, 1000.000000000000000 ) ;
#2368=ORIENTED_EDGE ( 'NONE', *, *, #10302, .T. ) ;
#2371=ORIENTED_EDGE ( 'NONE', *, *, #4079, .F. ) ;
#2383=ORIENTED_EDGE ( 'NONE', *, *, #7457, .F. ) ;
#2399=DIRECTION ( 'NONE',  ( 0.000000000000000000, 0.4999999999999983902, -0.8660254037844395958 ) ) ;
#2408=MECHANICAL_DESIGN_GEOMETRIC_PRESENTATION_REPRESENTATION('',(#5855),#190);
#2429=DIRECTION ( 'NONE',  ( -1.000000000000000000, -0.000000000000000000, -0.000000000000000000 ) ) ;
#2441=ORIENTED_EDGE ( 'NONE', *, *, #7673, .T. ) ;
#2464=DIRECTION ( 'NONE',  ( -1.000000000000000000, -0.000000000000000000, -0.000000000000000000 ) ) ;
#2468=EDGE_CURVE ( 'NONE', #6417, #1603, #4514, .T. ) ;
#2476=DIRECTION ( 'NONE',  ( -0.7071067811865452413, 0.000000000000000000, 0.7071067811865497932 ) ) ;
#2487=ORIENTED_EDGE ( 'NONE', *, *, #8314, .T. ) ;
#2488=CIRCLE ( 'NONE', #9390, 5.057500000000000107 ) ;
#2492=CARTESIAN_POINT ( 'NONE',  ( -31.74999999999995737, 0.000000000000000000, 5.999999999999999112 ) ) ;
#2505=EDGE_LOOP ( 'NONE', ( #3068, #6088, #2939, #5402, #817 ) ) ;
#2518=CARTESIAN_POINT ( 'NONE',  ( 0.6000000000000033085, 1.102182119232617714E-15, -9.000000000000000000 ) ) ;
#2530=FACE_OUTER_BOUND ( 'NONE', #2673, .T. ) ;
#2531=EDGE_LOOP ( 'NONE', ( #3024, #8191, #7057 ) ) ;
#2536=ADVANCED_FACE ( 'NONE', ( #8450 ), #6683, .F. ) ;
#2569=CARTESIAN_POINT ( 'NONE',  ( 92.00000000000000000, 0.000000000000000000, 0.000000000000000000 ) ) ;
#2570=ADVANCED_FACE ( 'NONE', ( #2161 ), #5969, .T. ) ;
#2583=FACE_OUTER_BOUND ( 'NONE', #10214, .T. ) ;
#2596=EDGE_LOOP ( 'NONE', ( #5876, #9536, #2058, #3144 ) ) ;
#2612=VERTEX_POINT ( 'NONE', #10654 ) ;
#2645=DIRECTION ( 'NONE',  ( 0.000000000000000000, 0.000000000000000000, -1.000000000000000000 ) ) ;
#2667=CARTESIAN_POINT ( 'NONE',  ( 6.000000000000000000, 2.919948986426526005, -5.057500000000003659 ) ) ;
#2673=EDGE_LOOP ( 'NONE', ( #4096, #2288, #2487, #12201, #10564 ) ) ;
#2744=DIRECTION ( 'NONE',  ( 0.000000000000000000, 0.000000000000000000, 1.000000000000000000 ) ) ;
#2774=DIRECTION ( 'NONE',  ( -1.000000000000000000, -0.000000000000000000, -0.000000000000000000 ) ) ;
#2775=AXIS2_PLACEMENT_3D ( 'NONE', #10318, #5636, #9383 ) ;
#2785=AXIS2_PLACEMENT_3D ( 'NONE', #9678, #286, #10740 ) ;
#2805=CARTESIAN_POINT ( 'NONE',  ( 6.000000000000000000, -4.379923479639793449, 2.528750000000004494 ) ) ;
#2819=ORIENTED_EDGE ( 'NONE', *, *, #2018, .F. ) ;
#2838=VECTOR ( 'NONE', #5599, 1000.000000000000000 ) ;
#2842=DIRECTION ( 'NONE',  ( -1.000000000000000000, -0.000000000000000000, -0.000000000000000000 ) ) ;
#2861=CARTESIAN_POINT ( 'NONE',  ( 6.000000000000000000, 2.919948986426538884, 5.057499999999996554 ) ) ;
#2876=ORIENTED_EDGE ( 'NONE', *, *, #12116, .F. ) ;
#2905=DIRECTION ( 'NONE',  ( 0.000000000000000000, 0.4999999999999983902, -0.8660254037844395958 ) ) ;
#2928=VERTEX_POINT ( 'NONE', #4563 ) ;
#2939=ORIENTED_EDGE ( 'NONE', *, *, #8320, .T. ) ;
#2946=PRODUCT ( 'socket head cap screw_iso_ISO 4762 M12 x 80 - 36N', 'socket head cap screw_iso_ISO 4762 M12 x 80 - 36N', '', ( #4566 ) ) ;
#2958=VECTOR ( 'NONE', #3019, 1000.000000000000000 ) ;
#2961=CARTESIAN_POINT ( 'NONE',  ( 0.000000000000000000, 0.000000000000000000, 0.000000000000000000 ) ) ;
#2967=CARTESIAN_POINT ( 'NONE',  ( 6.000000000000000000, 5.839897972853064445, -8.673617379884035472E-15 ) ) ;
#2975=DIRECTION ( 'NONE',  ( 0.000000000000000000, 0.000000000000000000, 1.000000000000000000 ) ) ;
#3019=DIRECTION ( 'NONE',  ( 0.000000000000000000, 1.000000000000000000, -1.039664082171044875E-15 ) ) ;
#3024=ORIENTED_EDGE ( 'NONE', *, *, #8314, .F. ) ;
#3034=PLANE ( 'NONE',  #5887 ) ;
#3068=ORIENTED_EDGE ( 'NONE', *, *, #7234, .F. ) ;
#3083=EDGE_CURVE ( 'NONE', #2354, #5181, #8805, .T. ) ;
#3096=ORIENTED_EDGE ( 'NONE', *, *, #1774, .T. ) ;
#3115=ADVANCED_FACE ( 'NONE', ( #3920 ), #3034, .F. ) ;
#3123=EDGE_CURVE ( 'NONE', #6417, #2265, #4670, .T. ) ;
#3132=ORIENTED_EDGE ( 'NONE', *, *, #3083, .F. ) ;
#3133=CARTESIAN_POINT ( 'NONE',  ( 91.03600000000000136, 0.000000000000000000, 5.999999999999998224 ) ) ;
#3144=ORIENTED_EDGE ( 'NONE', *, *, #8073, .F. ) ;
#3146=AXIS2_PLACEMENT_3D ( 'NONE', #7576, #3852, #1946 ) ;
#3147=EDGE_LOOP ( 'NONE', ( #3216, #9096, #11161, #7060 ) ) ;
#3182=ORIENTED_EDGE ( 'NONE', *, *, #7196, .T. ) ;
#3191=CONICAL_SURFACE ( 'NONE', #4608, 5.035999999999999588, 0.7853981633974514986 ) ;
#3216=ORIENTED_EDGE ( 'NONE', *, *, #8359, .F. ) ;
#3241=ORIENTED_EDGE ( 'NONE', *, *, #697, .T. ) ;
#3323=AXIS2_PLACEMENT_3D ( 'NONE', #9168, #9358, #3385 ) ;
#3342=CIRCLE ( 'NONE', #11654, 8.400000000000000355 ) ;
#3362=EDGE_LOOP ( 'NONE', ( #282, #9226, #9843, #2371 ) ) ;
#3376=CARTESIAN_POINT ( 'NONE',  ( 92.00000000000000000, 0.000000000000000000, 5.035999999999999588 ) ) ;
#3377=AXIS2_PLACEMENT_3D ( 'NONE', #12111, #7282, #3534 ) ;
#3385=DIRECTION ( 'NONE',  ( 0.000000000000000000, 0.000000000000000000, 1.000000000000000000 ) ) ;
#3395=DIRECTION ( 'NONE',  ( 0.000000000000000000, 0.000000000000000000, -1.000000000000000000 ) ) ;
#3406=DIRECTION ( 'NONE',  ( 1.000000000000000000, 0.000000000000000000, 0.000000000000000000 ) ) ;
#3422=CARTESIAN_POINT ( 'NONE',  ( 6.000000000000000000, 0.000000000000000000, 0.000000000000000000 ) ) ;
#3496=ORIENTED_EDGE ( 'NONE', *, *, #9909, .T. ) ;
#3498=CARTESIAN_POINT ( 'NONE',  ( 92.00000000000000000, 6.167321280506070407E-16, -5.035999999999999588 ) ) ;
#3502=CIRCLE ( 'NONE', #6340, 5.057500000000000107 ) ;
#3534=DIRECTION ( 'NONE',  ( 0.000000000000000000, 0.000000000000000000, -1.000000000000000000 ) ) ;
#3567=DIRECTION ( 'NONE',  ( 0.000000000000000000, 0.000000000000000000, 1.000000000000000000 ) ) ;
#3568=CYLINDRICAL_SURFACE ( 'NONE', #10816, 9.000000000000000000 ) ;
#3573=FACE_OUTER_BOUND ( 'NONE', #11963, .T. ) ;
#3603=DIRECTION ( 'NONE',  ( 0.000000000000000000, 0.4999999999999984457, -0.8660254037844394848 ) ) ;
#3632=LINE ( 'NONE', #4713, #899 ) ;
#3644=DIRECTION ( 'NONE',  ( -0.5000000000000046629, 0.000000000000000000, 0.8660254037844359321 ) ) ;
#3656=ADVANCED_FACE ( 'NONE', ( #6422 ), #8269, .T. ) ;
#3693=DIRECTION ( 'NONE',  ( 1.000000000000000000, 0.000000000000000000, 0.000000000000000000 ) ) ;
#3717=FACE_OUTER_BOUND ( 'NONE', #7893, .T. ) ;
#3768=CARTESIAN_POINT ( 'NONE',  ( 6.000000000000000000, 5.258101095580058680E-15, 5.057500000000000107 ) ) ;
#3769=EDGE_CURVE ( 'NONE', #174, #2354, #11617, .T. ) ;
#3791=DIRECTION ( 'NONE',  ( 0.000000000000000000, -1.000000000000000000, 1.039664082171044875E-15 ) ) ;
#3806=EDGE_LOOP ( 'NONE', ( #3808, #2819 ) ) ;
#3808=ORIENTED_EDGE ( 'NONE', *, *, #1641, .F. ) ;
#3823=DIRECTION ( 'NONE',  ( -0.000000000000000000, 0.8660254037844395958, 0.4999999999999983902 ) ) ;
#3845=FACE_OUTER_BOUND ( 'NONE', #4564, .T. ) ;
#3848=EDGE_LOOP ( 'NONE', ( #8448, #5912, #3182 ) ) ;
#3852=DIRECTION ( 'NONE',  ( -1.000000000000000000, -0.000000000000000000, -0.000000000000000000 ) ) ;
#3856=CARTESIAN_POINT ( 'NONE',  ( 6.000000000000000000, 2.919948986426526005, -5.057500000000003659 ) ) ;
#3886=ORIENTED_EDGE ( 'NONE', *, *, #8320, .F. ) ;
#3903=FACE_OUTER_BOUND ( 'NONE', #3806, .T. ) ;
#3909=APPLICATION_CONTEXT ( 'automotive_design' ) ;
#3912=ADVANCED_FACE ( 'NONE', ( #5276 ), #9149, .T. ) ;
#3920=FACE_OUTER_BOUND ( 'NONE', #5666, .T. ) ;
#4014=ORIENTED_EDGE ( 'NONE', *, *, #8243, .T. ) ;
#4020=DIRECTION ( 'NONE',  ( 0.000000000000000000, 0.000000000000000000, 1.000000000000000000 ) ) ;
#4030=DIRECTION ( 'NONE',  ( 0.000000000000000000, 0.000000000000000000, 1.000000000000000000 ) ) ;
#4061=FACE_OUTER_BOUND ( 'NONE', #901, .T. ) ;
#4067=VECTOR ( 'NONE', #6791, 1000.000000000000000 ) ;
#4077=DIRECTION ( 'NONE',  ( 0.000000000000000000, 0.4999999999999983902, -0.8660254037844395958 ) ) ;
#4079=EDGE_CURVE ( 'NONE', #5036, #11133, #8337, .T. ) ;
#4096=ORIENTED_EDGE ( 'NONE', *, *, #7443, .F. ) ;
#4111=ORIENTED_EDGE ( 'NONE', *, *, #5665, .F. ) ;
#4144=LINE ( 'NONE', #8837, #7908 ) ;
#4181=ADVANCED_FACE ( 'NONE', ( #10271 ), #819, .T. ) ;
#4193=EDGE_LOOP ( 'NONE', ( #3096, #6299 ) ) ;
#4226=ORIENTED_EDGE ( 'NONE', *, *, #3123, .T. ) ;
#4228=ORIENTED_EDGE ( 'NONE', *, *, #2231, .T. ) ;
#4253=VERTEX_POINT ( 'NONE', #1648 ) ;
#4292=ADVANCED_BREP_SHAPE_REPRESENTATION ( '', ( #1830, #9021 ), #1096 ) ;
#4304=LINE ( 'NONE', #8181, #2367 ) ;
#4334=FACE_OUTER_BOUND ( 'NONE', #1066, .T. ) ;
#4356=DIRECTION ( 'NONE',  ( -1.000000000000000000, -0.000000000000000000, -0.000000000000000000 ) ) ;
#4360=CARTESIAN_POINT ( 'NONE',  ( 6.000000000000000000, -5.839897972853060892, 7.806255641895631925E-15 ) ) ;
#4390=TOROIDAL_SURFACE ( 'NONE', #12486, 8.400000000000000355, 0.5999999999999999778 ) ;
#4391=ORIENTED_EDGE ( 'NONE', *, *, #11469, .F. ) ;
#4420=CARTESIAN_POINT ( 'NONE',  ( 0.6000000000000033085, 0.000000000000000000, 0.000000000000000000 ) ) ;
#4487=ORIENTED_EDGE ( 'NONE', *, *, #9521, .T. ) ;
#4497=CARTESIAN_POINT ( 'NONE',  ( -31.74999999999995737, 1.102182119232617714E-15, -9.000000000000000000 ) ) ;
#4498=PLANE ( 'NONE',  #590 ) ;
#4501=ORIENTED_EDGE ( 'NONE', *, *, #5303, .F. ) ;
#4510=CARTESIAN_POINT ( 'NONE',  ( 0.000000000000000000, -5.839897972853060892, 7.806255641895631925E-15 ) ) ;
#4514=LINE ( 'NONE', #3498, #2838 ) ;
#4519=ADVANCED_FACE ( 'NONE', ( #1244 ), #6039, .T. ) ;
#4530=CARTESIAN_POINT ( 'NONE',  ( 6.000000000000000000, 4.379923479639802331, 2.528749999999992948 ) ) ;
#4540=CARTESIAN_POINT ( 'NONE',  ( 12.00000000000000000, 0.000000000000000000, -6.599999999999998757 ) ) ;
#4541=EDGE_CURVE ( 'NONE', #2307, #11430, #9937, .T. ) ;
#4563=CARTESIAN_POINT ( 'NONE',  ( 0.000000000000000000, -2.919948986426523341, 5.057500000000002771 ) ) ;
#4564=EDGE_LOOP ( 'NONE', ( #5799, #1343 ) ) ;
#4566=PRODUCT_CONTEXT ( 'NONE', #3909, 'mechanical' ) ;
#4577=ADVANCED_FACE ( 'NONE', ( #105 ), #7901, .T. ) ;
#4608=AXIS2_PLACEMENT_3D ( 'NONE', #2569, #4356, #12159 ) ;
#4648=DIRECTION ( 'NONE',  ( -1.000000000000000000, -0.000000000000000000, -0.000000000000000000 ) ) ;
#4655=EDGE_LOOP ( 'NONE', ( #5702, #9321, #4699, #2094 ) ) ;
#4670=CIRCLE ( 'NONE', #1442, 5.035999999999999588 ) ;
#4699=ORIENTED_EDGE ( 'NONE', *, *, #4079, .T. ) ;
#4706=DIRECTION ( 'NONE',  ( 0.000000000000000000, 0.000000000000000000, 1.000000000000000000 ) ) ;
#4713=CARTESIAN_POINT ( 'NONE',  ( 6.000000000000000000, -2.919948986426523341, 5.057500000000002771 ) ) ;
#4725=LINE ( 'NONE', #733, #7784 ) ;
#4730=ORIENTED_EDGE ( 'NONE', *, *, #8073, .T. ) ;
#4746=DIRECTION ( 'NONE',  ( 0.000000000000000000, 1.000000000000000000, -1.224646799147353207E-16 ) ) ;
#4754=CARTESIAN_POINT ( 'NONE',  ( 6.000000000000000000, 2.919948986426538884, 5.057499999999996554 ) ) ;
#4766=CIRCLE ( 'NONE', #3146, 5.057500000000000107 ) ;
#4768=DIRECTION ( 'NONE',  ( 0.000000000000000000, 0.000000000000000000, 1.000000000000000000 ) ) ;
#4774=CIRCLE ( 'NONE', #7816, 9.000000000000000000 ) ;
#4777=DIRECTION ( 'NONE',  ( -1.000000000000000000, -0.000000000000000000, -0.000000000000000000 ) ) ;
#4781=CARTESIAN_POINT ( 'NONE',  ( 0.000000000000000000, -2.919948986426538440, -5.057499999999997442 ) ) ;
#4783=ORIENTED_EDGE ( 'NONE', *, *, #12173, .F. ) ;
#4798=DIRECTION ( 'NONE',  ( -1.000000000000000000, -0.000000000000000000, -0.000000000000000000 ) ) ;
#4826=AXIS2_PLACEMENT_3D ( 'NONE', #6881, #10745, #5937 ) ;
#4886=ADVANCED_FACE ( 'NONE', ( #3573 ), #7448, .F. ) ;
#4923=CARTESIAN_POINT ( 'NONE',  ( 92.00000000000000000, 0.000000000000000000, 0.000000000000000000 ) ) ;
#4925=FACE_BOUND ( 'NONE', #4193, .T. ) ;
#4945=VECTOR ( 'NONE', #2464, 1000.000000000000000 ) ;
#4959=ORIENTED_EDGE ( 'NONE', *, *, #9521, .F. ) ;
#4975=CARTESIAN_POINT ( 'NONE',  ( -31.74999999999995737, 0.000000000000000000, 9.000000000000000000 ) ) ;
#4991=DIRECTION ( 'NONE',  ( 0.000000000000000000, 0.000000000000000000, -1.000000000000000000 ) ) ;
#4996=DIRECTION ( 'NONE',  ( 0.000000000000000000, 0.000000000000000000, 1.000000000000000000 ) ) ;
#5020=PLANE ( 'NONE',  #1529 ) ;
#5036=VERTEX_POINT ( 'NONE', #1172 ) ;
#5054=ORIENTED_EDGE ( 'NONE', *, *, #2174, .T. ) ;
#5063=CIRCLE ( 'NONE', #12149, 5.999999999999998224 ) ;
#5075=ADVANCED_FACE ( 'NONE', ( #10669 ), #10731, .T. ) ;
#5116=ORIENTED_EDGE ( 'NONE', *, *, #11659, .F. ) ;
#5135=AXIS2_PLACEMENT_3D ( 'NONE', #6026, #6779, #11543 ) ;
#5181=VERTEX_POINT ( 'NONE', #11157 ) ;
#5184=EDGE_LOOP ( 'NONE', ( #2383, #11757, #4391 ) ) ;
#5191=TOROIDAL_SURFACE ( 'NONE', #10844, 6.599999999999998757, 0.5999999999999999778 ) ;
#5255=DIRECTION ( 'NONE',  ( 1.000000000000000000, 0.000000000000000000, 0.000000000000000000 ) ) ;
#5276=FACE_OUTER_BOUND ( 'NONE', #10956, .T. ) ;
#5280=ADVANCED_FACE ( 'NONE', ( #11350 ), #12528, .T. ) ;
#5303=EDGE_CURVE ( 'NONE', #409, #9559, #752, .T. ) ;
#5319=CARTESIAN_POINT ( 'NONE',  ( 0.6000000000000033085, 0.000000000000000000, 8.400000000000000355 ) ) ;
#5356=LINE ( 'NONE', #12080, #11642 ) ;
#5360=EDGE_CURVE ( 'NONE', #9553, #10329, #12138, .T. ) ;
#5398=ORIENTED_EDGE ( 'NONE', *, *, #9978, .F. ) ;
#5402=ORIENTED_EDGE ( 'NONE', *, *, #7457, .T. ) ;
#5489=DIRECTION ( 'NONE',  ( 0.000000000000000000, -0.5000000000000012212, -0.8660254037844380415 ) ) ;
#5564=CARTESIAN_POINT ( 'NONE',  ( 0.000000000000000000, 0.000000000000000000, 0.000000000000000000 ) ) ;
#5567=DIRECTION ( 'NONE',  ( -1.000000000000000000, -0.000000000000000000, -0.000000000000000000 ) ) ;
#5574=PLANE ( 'NONE',  #7424 ) ;
#5582=DIRECTION ( 'NONE',  ( 0.000000000000000000, 0.000000000000000000, 1.000000000000000000 ) ) ;
#5589=AXIS2_PLACEMENT_3D ( 'NONE', #10686, #2127, #4991 ) ;
#5599=DIRECTION ( 'NONE',  ( -0.7071067811865452413, 8.659560562354961208E-17, -0.7071067811865497932 ) ) ;
#5607=DIRECTION ( 'NONE',  ( 0.000000000000000000, -0.4999999999999985012, 0.8660254037844394848 ) ) ;
#5612=DIRECTION ( 'NONE',  ( 0.000000000000000000, 1.000000000000000000, -1.039664082171044875E-15 ) ) ;
#5616=VERTEX_POINT ( 'NONE', #4360 ) ;
#5617=ADVANCED_FACE ( 'NONE', ( #12223 ), #12040, .T. ) ;
#5636=DIRECTION ( 'NONE',  ( 0.000000000000000000, 0.8660254037844379305, -0.5000000000000012212 ) ) ;
#5639=CARTESIAN_POINT ( 'NONE',  ( 12.59999999999999964, 8.082668874372530033E-16, 6.599999999999998757 ) ) ;
#5646=CIRCLE ( 'NONE', #7263, 9.000000000000000000 ) ;
#5649=AXIS2_PLACEMENT_3D ( 'NONE', #11817, #3823, #2043 ) ;
#5665=EDGE_CURVE ( 'NONE', #1603, #5036, #7084, .T. ) ;
#5666=EDGE_LOOP ( 'NONE', ( #695, #4783, #743, #10363, #12092 ) ) ;
#5702=ORIENTED_EDGE ( 'NONE', *, *, #5360, .F. ) ;
#5729=CARTESIAN_POINT ( 'NONE',  ( 6.000000000000000000, 2.919948986426540660, 5.057499999999996554 ) ) ;
#5757=AXIS2_PLACEMENT_3D ( 'NONE', #10803, #1116, #4020 ) ;
#5799=ORIENTED_EDGE ( 'NONE', *, *, #8944, .T. ) ;
#5831=CARTESIAN_POINT ( 'NONE',  ( 6.000000000000000000, -2.919948986426523341, 5.057500000000002771 ) ) ;
#5837=CARTESIAN_POINT ( 'NONE',  ( 6.000000000000000000, 0.000000000000000000, 0.000000000000000000 ) ) ;
#5855=STYLED_ITEM('',(#12591),#1830);
#5876=ORIENTED_EDGE ( 'NONE', *, *, #791, .T. ) ;
#5887=AXIS2_PLACEMENT_3D ( 'NONE', #5831, #9830, #2076 ) ;
#5906=AXIS2_PLACEMENT_3D ( 'NONE', #4754, #7612, #10452 ) ;
#5910=VERTEX_POINT ( 'NONE', #11301 ) ;
#5912=ORIENTED_EDGE ( 'NONE', *, *, #2205, .F. ) ;
#5913=VERTEX_POINT ( 'NONE', #4510 ) ;
#5937=DIRECTION ( 'NONE',  ( 0.000000000000000000, 0.000000000000000000, 1.000000000000000000 ) ) ;
#5950=AXIS2_PLACEMENT_3D ( 'NONE', #907, #4777, #12269 ) ;
#5960=LINE ( 'NONE', #9836, #11890 ) ;
#5961=CARTESIAN_POINT ( 'NONE',  ( 6.000000000000000000, 0.000000000000000000, 0.000000000000000000 ) ) ;
#5969=PLANE ( 'NONE',  #9334 ) ;
#5988=DIRECTION ( 'NONE',  ( 0.000000000000000000, -0.5000000000000011102, -0.8660254037844379305 ) ) ;
#6003=CIRCLE ( 'NONE', #9653, 9.000000000000000000 ) ;
#6017=VECTOR ( 'NONE', #8106, 1000.000000000000000 ) ;
#6026=CARTESIAN_POINT ( 'NONE',  ( 0.6000000000000033085, 1.028703311283776586E-15, -8.400000000000000355 ) ) ;
#6039=CONICAL_SURFACE ( 'NONE', #6634, 5.035999999999999588, 0.7853981633974514986 ) ;
#6065=DIRECTION ( 'NONE',  ( 0.000000000000000000, 0.000000000000000000, 1.000000000000000000 ) ) ;
#6071=DIRECTION ( 'NONE',  ( -1.000000000000000000, -0.000000000000000000, -0.000000000000000000 ) ) ;
#6080=LINE ( 'NONE', #2967, #7235 ) ;
#6088=ORIENTED_EDGE ( 'NONE', *, *, #7443, .T. ) ;
#6167=CIRCLE ( 'NONE', #10216, 5.999999999999999112 ) ;
#6190=ORIENTED_EDGE ( 'NONE', *, *, #8359, .T. ) ;
#6203=DIRECTION ( 'NONE',  ( -1.000000000000000000, -0.000000000000000000, -0.000000000000000000 ) ) ;
#6248=AXIS2_PLACEMENT_3D ( 'NONE', #11318, #846, #5612 ) ;
#6286=VECTOR ( 'NONE', #11637, 1000.000000000000000 ) ;
#6299=ORIENTED_EDGE ( 'NONE', *, *, #9469, .T. ) ;
#6311=ADVANCED_FACE ( 'NONE', ( #10154 ), #4498, .T. ) ;
#6319=DIRECTION ( 'NONE',  ( -1.000000000000000000, -0.000000000000000000, -0.000000000000000000 ) ) ;
#6340=AXIS2_PLACEMENT_3D ( 'NONE', #5961, #9837, #491 ) ;
#6348=( NAMED_UNIT ( * ) SI_UNIT ( $, .STERADIAN. ) SOLID_ANGLE_UNIT ( ) );
#6363=CARTESIAN_POINT ( 'NONE',  ( 6.000000000000000000, 2.919948986426538884, 5.057499999999996554 ) ) ;
#6382=AXIS2_PLACEMENT_3D ( 'NONE', #5319, #6754, #12349 ) ;
#6391=DIRECTION ( 'NONE',  ( 1.000000000000000000, 0.000000000000000000, 0.000000000000000000 ) ) ;
#6394=AXIS2_PLACEMENT_3D ( 'NONE', #334, #2097, #1224 ) ;
#6417=VERTEX_POINT ( 'NONE', #11411 ) ;
#6422=FACE_OUTER_BOUND ( 'NONE', #623, .T. ) ;
#6428=CARTESIAN_POINT ( 'NONE',  ( 6.000000000000000000, 0.000000000000000000, 0.000000000000000000 ) ) ;
#6444=EDGE_CURVE ( 'NONE', #11432, #6932, #8616, .T. ) ;
#6456=LINE ( 'NONE', #560, #7636 ) ;
#6457=CARTESIAN_POINT ( 'NONE',  ( 6.000000000000000000, 4.379923479639795225, -2.528750000000006271 ) ) ;
#6488=FACE_OUTER_BOUND ( 'NONE', #8408, .T. ) ;
#6503=AXIS2_PLACEMENT_3D ( 'NONE', #10985, #12000, #11938 ) ;
#6508=CARTESIAN_POINT ( 'NONE',  ( 6.000000000000000000, -2.919948986426523341, 5.057500000000002771 ) ) ;
#6528=DIRECTION ( 'NONE',  ( 0.000000000000000000, -1.000000000000000000, 1.039664082171044875E-15 ) ) ;
#6544=DIRECTION ( 'NONE',  ( -1.000000000000000000, -0.000000000000000000, -0.000000000000000000 ) ) ;
#6566=DIRECTION ( 'NONE',  ( -1.000000000000000000, -0.000000000000000000, -0.000000000000000000 ) ) ;
#6581=DIRECTION ( 'NONE',  ( 0.000000000000000000, 0.000000000000000000, 1.000000000000000000 ) ) ;
#6622=CARTESIAN_POINT ( 'NONE',  ( 6.000000000000000000, -2.919948986426523341, 5.057500000000002771 ) ) ;
#6634=AXIS2_PLACEMENT_3D ( 'NONE', #4923, #8724, #6065 ) ;
#6636=CYLINDRICAL_SURFACE ( 'NONE', #10667, 5.999999999999999112 ) ;
#6682=ORIENTED_EDGE ( 'NONE', *, *, #2231, .F. ) ;
#6683=CONICAL_SURFACE ( 'NONE', #7496, 5.057500000000000107, 1.047197551196592302 ) ;
#6710=VERTEX_POINT ( 'NONE', #2518 ) ;
#6744=( NAMED_UNIT ( * ) SI_UNIT ( $, .STERADIAN. ) SOLID_ANGLE_UNIT ( ) );
#6748=DIRECTION ( 'NONE',  ( 0.000000000000000000, 1.000000000000000000, -1.039664082171044875E-15 ) ) ;
#6749=VECTOR ( 'NONE', #5567, 1000.000000000000000 ) ;
#6754=DIRECTION ( 'NONE',  ( 0.000000000000000000, -1.000000000000000000, 0.000000000000000000 ) ) ;
#6760=VECTOR ( 'NONE', #5607, 1000.000000000000000 ) ;
#6777=UNCERTAINTY_MEASURE_WITH_UNIT (LENGTH_MEASURE( 1.000000000000000082E-05 ), #2294, 'distance_accuracy_value', 'NONE');
#6779=DIRECTION ( 'NONE',  ( -0.000000000000000000, 1.000000000000000000, 1.224646799147353207E-16 ) ) ;
#6791=DIRECTION ( 'NONE',  ( -1.000000000000000000, -0.000000000000000000, -0.000000000000000000 ) ) ;
#6804=ORIENTED_EDGE ( 'NONE', *, *, #9909, .F. ) ;
#6813=DIRECTION ( 'NONE',  ( -0.5000000000000046629, 1.060575238724903587E-16, -0.8660254037844359321 ) ) ;
#6823=PLANE ( 'NONE',  #5589 ) ;
#6877=CARTESIAN_POINT ( 'NONE',  ( 6.000000000000000000, 6.193651186687738874E-16, -5.057500000000000107 ) ) ;
#6881=CARTESIAN_POINT ( 'NONE',  ( 6.000000000000000000, 2.919948986426538884, 5.057499999999996554 ) ) ;
#6932=VERTEX_POINT ( 'NONE', #8602 ) ;
#6935=LINE ( 'NONE', #6877, #11215 ) ;
#6949=ORIENTED_EDGE ( 'NONE', *, *, #11393, .T. ) ;
#6966=EDGE_CURVE ( 'NONE', #4253, #2928, #1934, .T. ) ;
#7021=DIRECTION ( 'NONE',  ( -1.000000000000000000, -0.000000000000000000, -0.000000000000000000 ) ) ;
#7043=VERTEX_POINT ( 'NONE', #8413 ) ;
#7057=ORIENTED_EDGE ( 'NONE', *, *, #1954, .F. ) ;
#7060=ORIENTED_EDGE ( 'NONE', *, *, #11108, .F. ) ;
#7061=CIRCLE ( 'NONE', #995, 6.599999999999998757 ) ;
#7074=CARTESIAN_POINT ( 'NONE',  ( 6.000000000000000000, 5.839897972853064445, -8.673617379884035472E-15 ) ) ;
#7078=EDGE_LOOP ( 'NONE', ( #1065, #4226, #4730, #9116 ) ) ;
#7081=CARTESIAN_POINT ( 'NONE',  ( 0.6000000000000033085, 0.000000000000000000, 0.000000000000000000 ) ) ;
#7084=LINE ( 'NONE', #10965, #9505 ) ;
#7136=VERTEX_POINT ( 'NONE', #3768 ) ;
#7189=DIRECTION ( 'NONE',  ( 0.000000000000000000, 0.000000000000000000, 1.000000000000000000 ) ) ;
#7196=EDGE_CURVE ( 'NONE', #4253, #7136, #9556, .T. ) ;
#7209=DIRECTION ( 'NONE',  ( 0.000000000000000000, 0.000000000000000000, -1.000000000000000000 ) ) ;
#7234=EDGE_CURVE ( 'NONE', #8699, #7136, #4725, .T. ) ;
#7235=VECTOR ( 'NONE', #10894, 999.9999999999998863 ) ;
#7263=AXIS2_PLACEMENT_3D ( 'NONE', #10749, #8852, #4030 ) ;
#7282=DIRECTION ( 'NONE',  ( -1.000000000000000000, -0.000000000000000000, -0.000000000000000000 ) ) ;
#7368=CIRCLE ( 'NONE', #11630, 5.057500000000000107 ) ;
#7424=AXIS2_PLACEMENT_3D ( 'NONE', #11211, #10146, #1457 ) ;
#7443=EDGE_CURVE ( 'NONE', #8699, #6932, #6935, .T. ) ;
#7447=DIRECTION ( 'NONE',  ( 0.000000000000000000, -0.5000000000000011102, -0.8660254037844379305 ) ) ;
#7448=PLANE ( 'NONE',  #6248 ) ;
#7457=EDGE_CURVE ( 'NONE', #409, #7687, #12041, .T. ) ;
#7493=EDGE_CURVE ( 'NONE', #10109, #6932, #7368, .T. ) ;
#7496=AXIS2_PLACEMENT_3D ( 'NONE', #12319, #202, #8633 ) ;
#7516=CARTESIAN_POINT ( 'NONE',  ( 6.000000000000000000, -2.919948986426523341, 5.057500000000002771 ) ) ;
#7518=EDGE_CURVE ( 'NONE', #2354, #2307, #9293, .T. ) ;
#7519=ORIENTED_EDGE ( 'NONE', *, *, #11659, .T. ) ;
#7535=EDGE_CURVE ( 'NONE', #938, #10109, #8793, .T. ) ;
#7558=ORIENTED_EDGE ( 'NONE', *, *, #12046, .T. ) ;
#7569=LINE ( 'NONE', #1909, #6760 ) ;
#7572=VECTOR ( 'NONE', #6748, 1000.000000000000000 ) ;
#7576=CARTESIAN_POINT ( 'NONE',  ( 6.000000000000000000, 0.000000000000000000, 0.000000000000000000 ) ) ;
#7609=EDGE_CURVE ( 'NONE', #438, #1603, #11418, .T. ) ;
#7612=DIRECTION ( 'NONE',  ( -1.000000000000000000, 0.000000000000000000, 0.000000000000000000 ) ) ;
#7636=VECTOR ( 'NONE', #9323, 1000.000000000000000 ) ;
#7663=DIRECTION ( 'NONE',  ( 0.000000000000000000, 0.000000000000000000, 1.000000000000000000 ) ) ;
#7673=EDGE_CURVE ( 'NONE', #174, #938, #7569, .T. ) ;
#7678=ADVANCED_FACE ( 'NONE', ( #6488 ), #3568, .T. ) ;
#7687=VERTEX_POINT ( 'NONE', #2805 ) ;
#7694=CARTESIAN_POINT ( 'NONE',  ( -31.74999999999995737, 0.000000000000000000, 0.000000000000000000 ) ) ;
#7712=DIRECTION ( 'NONE',  ( 0.000000000000000000, 0.000000000000000000, 1.000000000000000000 ) ) ;
#7720=EDGE_LOOP ( 'NONE', ( #8316, #6190, #1454, #2876 ) ) ;
#7726=AXIS2_PLACEMENT_3D ( 'NONE', #6363, #408, #10285 ) ;
#7764=LINE ( 'NONE', #4975, #6286 ) ;
#7784=VECTOR ( 'NONE', #3644, 1000.000000000000000 ) ;
#7796=DIRECTION ( 'NONE',  ( -1.000000000000000000, -0.000000000000000000, -0.000000000000000000 ) ) ;
#7797=VERTEX_POINT ( 'NONE', #9916 ) ;
#7816=AXIS2_PLACEMENT_3D ( 'NONE', #4420, #6391, #12168 ) ;
#7893=EDGE_LOOP ( 'NONE', ( #4111, #3241, #10268, #1734 ) ) ;
#7901=PLANE ( 'NONE',  #4826 ) ;
#7908=VECTOR ( 'NONE', #4077, 1000.000000000000000 ) ;
#7963=CIRCLE ( 'NONE', #5135, 0.5999999999999998668 ) ;
#7975=LINE ( 'NONE', #488, #11332 ) ;
#8073=EDGE_CURVE ( 'NONE', #2265, #438, #8198, .T. ) ;
#8106=DIRECTION ( 'NONE',  ( 0.000000000000000000, 1.000000000000000000, -1.039664082171044875E-15 ) ) ;
#8145=CARTESIAN_POINT ( 'NONE',  ( 0.000000000000000000, 5.839897972853064445, -8.673617379884035472E-15 ) ) ;
#8146=ORIENTED_EDGE ( 'NONE', *, *, #6966, .F. ) ;
#8165=ORIENTED_EDGE ( 'NONE', *, *, #791, .F. ) ;
#8170=VECTOR ( 'NONE', #6528, 1000.000000000000000 ) ;
#8181=CARTESIAN_POINT ( 'NONE',  ( 0.000000000000000000, -5.839897972853060892, 7.806255641895631925E-15 ) ) ;
#8191=ORIENTED_EDGE ( 'NONE', *, *, #1458, .T. ) ;
#8198=LINE ( 'NONE', #11943, #1681 ) ;
#8243=EDGE_CURVE ( 'NONE', #6932, #9559, #8441, .T. ) ;
#8269=PLANE ( 'NONE',  #7726 ) ;
#8311=LINE ( 'NONE', #4497, #4945 ) ;
#8314=EDGE_CURVE ( 'NONE', #7136, #938, #3502, .T. ) ;
#8316=ORIENTED_EDGE ( 'NONE', *, *, #1196, .F. ) ;
#8320=EDGE_CURVE ( 'NONE', #6932, #409, #2488, .T. ) ;
#8337=CIRCLE ( 'NONE', #10348, 0.5999999999999998668 ) ;
#8359=EDGE_CURVE ( 'NONE', #6710, #5910, #7963, .T. ) ;
#8408=EDGE_LOOP ( 'NONE', ( #5116, #9577, #4228, #7558 ) ) ;
#8413=CARTESIAN_POINT ( 'NONE',  ( 0.000000000000000000, 0.000000000000000000, 8.400000000000000355 ) ) ;
#8441=LINE ( 'NONE', #2667, #8170 ) ;
#8448=ORIENTED_EDGE ( 'NONE', *, *, #10768, .F. ) ;
#8450=FACE_OUTER_BOUND ( 'NONE', #2505, .T. ) ;
#8543=CARTESIAN_POINT ( 'NONE',  ( 6.000000000000000000, 2.919948986426540660, 5.057499999999996554 ) ) ;
#8592=ORIENTED_EDGE ( 'NONE', *, *, #7609, .T. ) ;
#8602=CARTESIAN_POINT ( 'NONE',  ( 6.000000000000000000, -5.258101095580059469E-15, -5.057500000000000995 ) ) ;
#8616=LINE ( 'NONE', #3856, #10931 ) ;
#8633=DIRECTION ( 'NONE',  ( 0.000000000000000000, 0.000000000000000000, 1.000000000000000000 ) ) ;
#8636=ORIENTED_EDGE ( 'NONE', *, *, #9724, .F. ) ;
#8668=DIRECTION ( 'NONE',  ( -0.000000000000000000, 0.000000000000000000, 1.000000000000000000 ) ) ;
#8671=ADVANCED_FACE ( 'NONE', ( #1445 ), #3191, .T. ) ;
#8699=VERTEX_POINT ( 'NONE', #11200 ) ;
#8702=ORIENTED_EDGE ( 'NONE', *, *, #5303, .T. ) ;
#8724=DIRECTION ( 'NONE',  ( -1.000000000000000000, -0.000000000000000000, -0.000000000000000000 ) ) ;
#8792=LINE ( 'NONE', #9815, #339 ) ;
#8793=CIRCLE ( 'NONE', #3323, 5.057500000000000107 ) ;
#8805=LINE ( 'NONE', #9576, #11356 ) ;
#8837=CARTESIAN_POINT ( 'NONE',  ( 6.000000000000000000, -5.839897972853060892, 7.806255641895631925E-15 ) ) ;
#8852=DIRECTION ( 'NONE',  ( -1.000000000000000000, -0.000000000000000000, -0.000000000000000000 ) ) ;
#8857=APPLICATION_CONTEXT ( 'automotive_design' ) ;
#8944=EDGE_CURVE ( 'NONE', #7043, #5910, #10477, .T. ) ;
#8985=ORIENTED_EDGE ( 'NONE', *, *, #9066, .F. ) ;
#9008=AXIS2_PLACEMENT_3D ( 'NONE', #12042, #5255, #676 ) ;
#9021=AXIS2_PLACEMENT_3D ( 'NONE', #11433, #2744, #207 ) ;
#9066=EDGE_CURVE ( 'NONE', #438, #9553, #12205, .T. ) ;
#9083=EDGE_LOOP ( 'NONE', ( #3132, #9567, #2441, #1825, #11150 ) ) ;
#9096=ORIENTED_EDGE ( 'NONE', *, *, #12046, .F. ) ;
#9116=ORIENTED_EDGE ( 'NONE', *, *, #697, .F. ) ;
#9149=PLANE ( 'NONE',  #6503 ) ;
#9168=CARTESIAN_POINT ( 'NONE',  ( 6.000000000000000000, 0.000000000000000000, 0.000000000000000000 ) ) ;
#9178=DIRECTION ( 'NONE',  ( 0.000000000000000000, 0.000000000000000000, 1.000000000000000000 ) ) ;
#9189=FACE_OUTER_BOUND ( 'NONE', #3362, .T. ) ;
#9194=ORIENTED_EDGE ( 'NONE', *, *, #10302, .F. ) ;
#9209=DIRECTION ( 'NONE',  ( 0.000000000000000000, -1.000000000000000000, 0.000000000000000000 ) ) ;
#9226=ORIENTED_EDGE ( 'NONE', *, *, #5360, .T. ) ;
#9232=DIRECTION ( 'NONE',  ( -1.000000000000000000, -0.000000000000000000, -0.000000000000000000 ) ) ;
#9244=AXIS2_PLACEMENT_3D ( 'NONE', #2961, #11397, #8668 ) ;
#9249=ADVANCED_FACE ( 'NONE', ( #9356 ), #657, .T. ) ;
#9252=DIRECTION ( 'NONE',  ( 1.000000000000000000, 0.000000000000000000, 0.000000000000000000 ) ) ;
#9292=DIRECTION ( 'NONE',  ( -1.000000000000000000, -0.000000000000000000, -0.000000000000000000 ) ) ;
#9293=LINE ( 'NONE', #1608, #1892 ) ;
#9321=ORIENTED_EDGE ( 'NONE', *, *, #11393, .F. ) ;
#9323=DIRECTION ( 'NONE',  ( -1.000000000000000000, -0.000000000000000000, -0.000000000000000000 ) ) ;
#9334=AXIS2_PLACEMENT_3D ( 'NONE', #2861, #9779, #4768 ) ;
#9356=FACE_OUTER_BOUND ( 'NONE', #12505, .T. ) ;
#9358=DIRECTION ( 'NONE',  ( -1.000000000000000000, -0.000000000000000000, -0.000000000000000000 ) ) ;
#9378=FACE_OUTER_BOUND ( 'NONE', #4655, .T. ) ;
#9383=DIRECTION ( 'NONE',  ( 0.000000000000000000, 0.5000000000000012212, 0.8660254037844379305 ) ) ;
#9387=CARTESIAN_POINT ( 'NONE',  ( 0.6000000000000033085, 0.000000000000000000, 0.000000000000000000 ) ) ;
#9390=AXIS2_PLACEMENT_3D ( 'NONE', #5837, #11737, #9709 ) ;
#9410=CONICAL_SURFACE ( 'NONE', #12241, 5.057500000000000107, 1.047197551196592302 ) ;
#9469=EDGE_CURVE ( 'NONE', #10329, #11133, #12294, .T. ) ;
#9477=ADVANCED_FACE ( 'NONE', ( #2583 ), #5574, .T. ) ;
#9505=VECTOR ( 'NONE', #6203, 1000.000000000000000 ) ;
#9512=DIRECTION ( 'NONE',  ( 0.000000000000000000, 1.224646799147353207E-16, 1.000000000000000000 ) ) ;
#9521=EDGE_CURVE ( 'NONE', #5616, #5913, #6456, .T. ) ;
#9536=ORIENTED_EDGE ( 'NONE', *, *, #2468, .T. ) ;
#9547=DIRECTION ( 'NONE',  ( 0.000000000000000000, 0.000000000000000000, -1.000000000000000000 ) ) ;
#9553=VERTEX_POINT ( 'NONE', #684 ) ;
#9556=LINE ( 'NONE', #6622, #7572 ) ;
#9559=VERTEX_POINT ( 'NONE', #12358 ) ;
#9567=ORIENTED_EDGE ( 'NONE', *, *, #3769, .F. ) ;
#9576=CARTESIAN_POINT ( 'NONE',  ( 0.000000000000000000, 5.839897972853064445, -8.673617379884035472E-15 ) ) ;
#9577=ORIENTED_EDGE ( 'NONE', *, *, #2018, .T. ) ;
#9630=EDGE_LOOP ( 'NONE', ( #8165, #11309 ) ) ;
#9645=ADVANCED_FACE ( 'NONE', ( #370 ), #4390, .T. ) ;
#9653=AXIS2_PLACEMENT_3D ( 'NONE', #1561, #6319, #9178 ) ;
#9656=ORIENTED_EDGE ( 'NONE', *, *, #7518, .T. ) ;
#9678=CARTESIAN_POINT ( 'NONE',  ( 0.000000000000000000, 0.000000000000000000, 0.000000000000000000 ) ) ;
#9709=DIRECTION ( 'NONE',  ( 0.000000000000000000, 0.000000000000000000, 1.000000000000000000 ) ) ;
#9724=EDGE_CURVE ( 'NONE', #2928, #5181, #178, .T. ) ;
#9758=DIRECTION ( 'NONE',  ( 0.000000000000000000, 0.000000000000000000, 1.000000000000000000 ) ) ;
#9779=DIRECTION ( 'NONE',  ( -1.000000000000000000, 0.000000000000000000, 0.000000000000000000 ) ) ;
#9815=CARTESIAN_POINT ( 'NONE',  ( 6.000000000000000000, -2.919948986426538440, -5.057499999999997442 ) ) ;
#9830=DIRECTION ( 'NONE',  ( -0.000000000000000000, 1.039664082171044875E-15, 1.000000000000000000 ) ) ;
#9836=CARTESIAN_POINT ( 'NONE',  ( 0.000000000000000000, -2.919948986426523341, 5.057500000000002771 ) ) ;
#9837=DIRECTION ( 'NONE',  ( -1.000000000000000000, -0.000000000000000000, -0.000000000000000000 ) ) ;
#9843=ORIENTED_EDGE ( 'NONE', *, *, #1774, .F. ) ;
#9909=EDGE_CURVE ( 'NONE', #2928, #5913, #5960, .T. ) ;
#9916=CARTESIAN_POINT ( 'NONE',  ( 12.00000000000000355, 1.102182119232617714E-15, -9.000000000000000000 ) ) ;
#9937=LINE ( 'NONE', #2123, #379 ) ;
#9938=ORIENTED_EDGE ( 'NONE', *, *, #7673, .F. ) ;
#9978=EDGE_CURVE ( 'NONE', #5913, #11430, #4304, .T. ) ;
#10004=ORIENTED_EDGE ( 'NONE', *, *, #3083, .T. ) ;
#10025=AXIS2_PLACEMENT_3D ( 'NONE', #1483, #2429, #4996 ) ;
#10073=ADVANCED_FACE ( 'NONE', ( #810 ), #10380, .F. ) ;
#10093=ORIENTED_EDGE ( 'NONE', *, *, #1575, .T. ) ;
#10109=VERTEX_POINT ( 'NONE', #6457 ) ;
#10116=ADVANCED_FACE ( 'NONE', ( #3717 ), #6636, .T. ) ;
#10146=DIRECTION ( 'NONE',  ( -1.000000000000000000, 0.000000000000000000, 0.000000000000000000 ) ) ;
#10154=FACE_OUTER_BOUND ( 'NONE', #9083, .T. ) ;
#10214=EDGE_LOOP ( 'NONE', ( #3886, #4014, #4501 ) ) ;
#10216=AXIS2_PLACEMENT_3D ( 'NONE', #11317, #3693, #9547 ) ;
#10257=EDGE_LOOP ( 'NONE', ( #10004, #8636, #3496, #10673, #71, #11167 ) ) ;
#10268=ORIENTED_EDGE ( 'NONE', *, *, #9066, .T. ) ;
#10271=FACE_OUTER_BOUND ( 'NONE', #2531, .T. ) ;
#10285=DIRECTION ( 'NONE',  ( 0.000000000000000000, 0.000000000000000000, 1.000000000000000000 ) ) ;
#10296=VECTOR ( 'NONE', #2905, 1000.000000000000000 ) ;
#10302=EDGE_CURVE ( 'NONE', #10109, #11432, #6080, .T. ) ;
#10304=CARTESIAN_POINT ( 'NONE',  ( 6.000000000000000000, 5.839897972853064445, -8.673617379884035472E-15 ) ) ;
#10318=CARTESIAN_POINT ( 'NONE',  ( 6.000000000000000000, 5.839897972853064445, -8.673617379884035472E-15 ) ) ;
#10329=VERTEX_POINT ( 'NONE', #306 ) ;
#10348=AXIS2_PLACEMENT_3D ( 'NONE', #1467, #9209, #516 ) ;
#10355=AXIS2_PLACEMENT_3D ( 'NONE', #10485, #12459, #10548 ) ;
#10363=ORIENTED_EDGE ( 'NONE', *, *, #7196, .F. ) ;
#10380=PLANE ( 'NONE',  #2775 ) ;
#10437=FACE_BOUND ( 'NONE', #10257, .T. ) ;
#10452=DIRECTION ( 'NONE',  ( 0.000000000000000000, 0.000000000000000000, 1.000000000000000000 ) ) ;
#10477=CIRCLE ( 'NONE', #2785, 8.400000000000000355 ) ;
#10485=CARTESIAN_POINT ( 'NONE',  ( 12.59999999999999964, 0.000000000000000000, 0.000000000000000000 ) ) ;
#10487=DIRECTION ( 'NONE',  ( 0.000000000000000000, 0.5000000000000011102, 0.8660254037844379305 ) ) ;
#10531=PRODUCT_DEFINITION ( 'UNKNOWN', '', #888, #10942 ) ;
#10534=ORIENTED_EDGE ( 'NONE', *, *, #6444, .F. ) ;
#10548=DIRECTION ( 'NONE',  ( 0.000000000000000000, 0.000000000000000000, -1.000000000000000000 ) ) ;
#10550=DIRECTION ( 'NONE',  ( 0.000000000000000000, 0.8660254037844380415, -0.5000000000000012212 ) ) ;
#10564=ORIENTED_EDGE ( 'NONE', *, *, #7493, .T. ) ;
#10574=CARTESIAN_POINT ( 'NONE',  ( 6.000000000000000000, -5.839897972853060892, 7.806255641895631925E-15 ) ) ;
#10612=AXIS2_PLACEMENT_3D ( 'NONE', #619, #11023, #497 ) ;
#10620=LINE ( 'NONE', #8543, #98 ) ;
#10654=CARTESIAN_POINT ( 'NONE',  ( 0.6000000000000033085, 0.000000000000000000, 9.000000000000000000 ) ) ;
#10659=CARTESIAN_POINT ( 'NONE',  ( 91.03600000000000136, 0.000000000000000000, 0.000000000000000000 ) ) ;
#10667=AXIS2_PLACEMENT_3D ( 'NONE', #11466, #2774, #7663 ) ;
#10669=FACE_OUTER_BOUND ( 'NONE', #2049, .T. ) ;
#10673=ORIENTED_EDGE ( 'NONE', *, *, #9978, .T. ) ;
#10686=CARTESIAN_POINT ( 'NONE',  ( 12.00000000000000178, 9.000000000000000000, 0.000000000000000000 ) ) ;
#10731=PLANE ( 'NONE',  #5649 ) ;
#10740=DIRECTION ( 'NONE',  ( 0.000000000000000000, 0.000000000000000000, 1.000000000000000000 ) ) ;
#10745=DIRECTION ( 'NONE',  ( -1.000000000000000000, 0.000000000000000000, 0.000000000000000000 ) ) ;
#10749=CARTESIAN_POINT ( 'NONE',  ( 12.00000000000000355, 0.000000000000000000, 0.000000000000000000 ) ) ;
#10751=CARTESIAN_POINT ( 'NONE',  ( 91.03600000000000136, 7.347880794884117764E-16, -5.999999999999998224 ) ) ;
#10764=DIRECTION ( 'NONE',  ( 0.000000000000000000, -0.4999999999999985012, 0.8660254037844394848 ) ) ;
#10768=EDGE_CURVE ( 'NONE', #7687, #7136, #4766, .T. ) ;
#10803=CARTESIAN_POINT ( 'NONE',  ( 6.000000000000000000, 0.000000000000000000, 0.000000000000000000 ) ) ;
#10815=SHAPE_REPRESENTATION ( 'socket head cap screw_iso_ISO 4762 M12 x 80 - 36N', ( #9021 ), #1096 ) ;
#10816=AXIS2_PLACEMENT_3D ( 'NONE', #7694, #4648, #11561 ) ;
#10844=AXIS2_PLACEMENT_3D ( 'NONE', #12227, #3406, #2645 ) ;
#10885=ORIENTED_EDGE ( 'NONE', *, *, #7535, .F. ) ;
#10891=VECTOR ( 'NONE', #9292, 1000.000000000000000 ) ;
#10894=DIRECTION ( 'NONE',  ( 0.000000000000000000, -0.5000000000000012212, -0.8660254037844380415 ) ) ;
#10931=VECTOR ( 'NONE', #3791, 1000.000000000000000 ) ;
#10942=PRODUCT_DEFINITION_CONTEXT ( 'detailed design', #8857, 'design' ) ;
#10952=DIRECTION ( 'NONE',  ( 0.000000000000000000, -0.4999999999999985012, 0.8660254037844394848 ) ) ;
#10956=EDGE_LOOP ( 'NONE', ( #10885, #9938, #11258 ) ) ;
#10965=CARTESIAN_POINT ( 'NONE',  ( -31.74999999999995737, 7.347880794884118750E-16, -5.999999999999999112 ) ) ;
#10985=CARTESIAN_POINT ( 'NONE',  ( 6.000000000000000000, 2.919948986426538884, 5.057499999999996554 ) ) ;
#11014=ORIENTED_EDGE ( 'NONE', *, *, #1196, .T. ) ;
#11022=CARTESIAN_POINT ( 'NONE',  ( 92.00000000000000000, 5.035999999999999588, 0.000000000000000000 ) ) ;
#11023=DIRECTION ( 'NONE',  ( 1.000000000000000000, 0.000000000000000000, 0.000000000000000000 ) ) ;
#11032=CIRCLE ( 'NONE', #6382, 0.5999999999999998668 ) ;
#11108=EDGE_CURVE ( 'NONE', #5910, #7043, #3342, .T. ) ;
#11133=VERTEX_POINT ( 'NONE', #4540 ) ;
#11136=ORIENTED_EDGE ( 'NONE', *, *, #4541, .T. ) ;
#11150=ORIENTED_EDGE ( 'NONE', *, *, #12173, .T. ) ;
#11157=CARTESIAN_POINT ( 'NONE',  ( 0.000000000000000000, 2.919948986426540660, 5.057499999999996554 ) ) ;
#11161=ORIENTED_EDGE ( 'NONE', *, *, #12116, .T. ) ;
#11167=ORIENTED_EDGE ( 'NONE', *, *, #7518, .F. ) ;
#11170=( NAMED_UNIT ( * ) PLANE_ANGLE_UNIT ( ) SI_UNIT ( $, .RADIAN. ) );
#11200=CARTESIAN_POINT ( 'NONE',  ( 8.919948986426568638, 0.000000000000000000, 0.000000000000000000 ) ) ;
#11211=CARTESIAN_POINT ( 'NONE',  ( 6.000000000000000000, 2.919948986426538884, 5.057499999999996554 ) ) ;
#11215=VECTOR ( 'NONE', #6813, 1000.000000000000000 ) ;
#11258=ORIENTED_EDGE ( 'NONE', *, *, #60, .T. ) ;
#11301=CARTESIAN_POINT ( 'NONE',  ( 0.000000000000000000, 1.065442715258197248E-15, -8.400000000000000355 ) ) ;
#11309=ORIENTED_EDGE ( 'NONE', *, *, #3123, .F. ) ;
#11317=CARTESIAN_POINT ( 'NONE',  ( 12.59999999999999964, 0.000000000000000000, 0.000000000000000000 ) ) ;
#11318=CARTESIAN_POINT ( 'NONE',  ( 6.000000000000000000, 2.919948986426526005, -5.057500000000003659 ) ) ;
#11324=CARTESIAN_POINT ( 'NONE',  ( 12.00000000000000178, 0.000000000000000000, 0.000000000000000000 ) ) ;
#11332=VECTOR ( 'NONE', #11779, 999.9999999999998863 ) ;
#11350=FACE_OUTER_BOUND ( 'NONE', #3147, .T. ) ;
#11356=VECTOR ( 'NONE', #10764, 1000.000000000000000 ) ;
#11393=EDGE_CURVE ( 'NONE', #5036, #9553, #6167, .T. ) ;
#11397=DIRECTION ( 'NONE',  ( -1.000000000000000000, 0.000000000000000000, -0.000000000000000000 ) ) ;
#11411=CARTESIAN_POINT ( 'NONE',  ( 92.00000000000000000, 6.757601037695094579E-16, -5.035999999999999588 ) ) ;
#11418=CIRCLE ( 'NONE', #5950, 5.999999999999998224 ) ;
#11430=VERTEX_POINT ( 'NONE', #4781 ) ;
#11432=VERTEX_POINT ( 'NONE', #845 ) ;
#11433=CARTESIAN_POINT ( 'NONE',  ( 0.000000000000000000, 0.000000000000000000, 0.000000000000000000 ) ) ;
#11460=CARTESIAN_POINT ( 'NONE',  ( 12.00000000000000355, 0.000000000000000000, 9.000000000000000000 ) ) ;
#11466=CARTESIAN_POINT ( 'NONE',  ( -31.74999999999995737, 0.000000000000000000, 0.000000000000000000 ) ) ;
#11468=DIRECTION ( 'NONE',  ( -1.000000000000000000, -0.000000000000000000, -0.000000000000000000 ) ) ;
#11469=EDGE_CURVE ( 'NONE', #7687, #5616, #3632, .T. ) ;
#11543=DIRECTION ( 'NONE',  ( 0.000000000000000000, -1.224646799147353207E-16, 1.000000000000000000 ) ) ;
#11561=DIRECTION ( 'NONE',  ( 0.000000000000000000, 0.000000000000000000, 1.000000000000000000 ) ) ;
#11571=( NAMED_UNIT ( * ) PLANE_ANGLE_UNIT ( ) SI_UNIT ( $, .RADIAN. ) );
#11617=LINE ( 'NONE', #1092, #4067 ) ;
#11630=AXIS2_PLACEMENT_3D ( 'NONE', #6428, #9232, #7189 ) ;
#11637=DIRECTION ( 'NONE',  ( -1.000000000000000000, -0.000000000000000000, -0.000000000000000000 ) ) ;
#11639=ORIENTED_EDGE ( 'NONE', *, *, #3769, .T. ) ;
#11642=VECTOR ( 'NONE', #470, 1000.000000000000000 ) ;
#11654=AXIS2_PLACEMENT_3D ( 'NONE', #5564, #6566, #7712 ) ;
#11659=EDGE_CURVE ( 'NONE', #7797, #6710, #8311, .T. ) ;
#11737=DIRECTION ( 'NONE',  ( -1.000000000000000000, -0.000000000000000000, -0.000000000000000000 ) ) ;
#11757=ORIENTED_EDGE ( 'NONE', *, *, #2174, .F. ) ;
#11779=DIRECTION ( 'NONE',  ( 0.000000000000000000, -0.5000000000000012212, -0.8660254037844380415 ) ) ;
#11793=DIRECTION ( 'NONE',  ( 0.000000000000000000, -0.5000000000000011102, -0.8660254037844379305 ) ) ;
#11801=ADVANCED_FACE ( 'NONE', ( #2530 ), #9410, .F. ) ;
#11817=CARTESIAN_POINT ( 'NONE',  ( 6.000000000000000000, -5.839897972853060892, 7.806255641895631925E-15 ) ) ;
#11841=CARTESIAN_POINT ( 'NONE',  ( 6.000000000000000000, -2.919948986426523341, 5.057500000000002771 ) ) ;
#11851=CIRCLE ( 'NONE', #9008, 9.000000000000000000 ) ;
#11890=VECTOR ( 'NONE', #11793, 1000.000000000000114 ) ;
#11929=AXIS2_PLACEMENT_3D ( 'NONE', #11022, #9252, #7209 ) ;
#11938=DIRECTION ( 'NONE',  ( 0.000000000000000000, 0.000000000000000000, 1.000000000000000000 ) ) ;
#11943=CARTESIAN_POINT ( 'NONE',  ( 92.00000000000000000, 0.000000000000000000, 5.035999999999999588 ) ) ;
#11963=EDGE_LOOP ( 'NONE', ( #11136, #1647, #1844, #10534, #1773 ) ) ;
#11989=CIRCLE ( 'NONE', #10355, 5.999999999999999112 ) ;
#12000=DIRECTION ( 'NONE',  ( -1.000000000000000000, 0.000000000000000000, 0.000000000000000000 ) ) ;
#12040=PLANE ( 'NONE',  #11929 ) ;
#12041=CIRCLE ( 'NONE', #5757, 5.057500000000000107 ) ;
#12042=CARTESIAN_POINT ( 'NONE',  ( 0.6000000000000033085, 0.000000000000000000, 0.000000000000000000 ) ) ;
#12046=EDGE_CURVE ( 'NONE', #2612, #6710, #11851, .T. ) ;
#12052=TOROIDAL_SURFACE ( 'NONE', #10612, 6.599999999999998757, 0.5999999999999999778 ) ;
#12080=CARTESIAN_POINT ( 'NONE',  ( 6.000000000000000000, 2.919948986426526005, -5.057500000000003659 ) ) ;
#12084=ADVANCED_FACE ( 'NONE', ( #9189 ), #12052, .F. ) ;
#12092=ORIENTED_EDGE ( 'NONE', *, *, #6966, .T. ) ;
#12111=CARTESIAN_POINT ( 'NONE',  ( 12.00000000000000178, 0.000000000000000000, 0.000000000000000000 ) ) ;
#12116=EDGE_CURVE ( 'NONE', #2612, #7043, #11032, .T. ) ;
#12138=CIRCLE ( 'NONE', #1989, 0.5999999999999998668 ) ;
#12149=AXIS2_PLACEMENT_3D ( 'NONE', #10659, #6544, #4706 ) ;
#12159=DIRECTION ( 'NONE',  ( 0.000000000000000000, 0.000000000000000000, 1.000000000000000000 ) ) ;
#12168=DIRECTION ( 'NONE',  ( 0.000000000000000000, 0.000000000000000000, 1.000000000000000000 ) ) ;
#12173=EDGE_CURVE ( 'NONE', #637, #5181, #10620, .T. ) ;
#12201=ORIENTED_EDGE ( 'NONE', *, *, #7535, .T. ) ;
#12205=LINE ( 'NONE', #2492, #10891 ) ;
#12223=FACE_OUTER_BOUND ( 'NONE', #9630, .T. ) ;
#12227=CARTESIAN_POINT ( 'NONE',  ( 12.59999999999999964, 0.000000000000000000, 0.000000000000000000 ) ) ;
#12241=AXIS2_PLACEMENT_3D ( 'NONE', #3422, #2842, #5582 ) ;
#12242=DIRECTION ( 'NONE',  ( 0.000000000000000000, -0.8660254037844395958, -0.4999999999999985012 ) ) ;
#12267=CARTESIAN_POINT ( 'NONE',  ( -31.74999999999995737, 0.000000000000000000, 0.000000000000000000 ) ) ;
#12269=DIRECTION ( 'NONE',  ( 0.000000000000000000, 0.000000000000000000, 1.000000000000000000 ) ) ;
#12270=VECTOR ( 'NONE', #10952, 1000.000000000000000 ) ;
#12294=CIRCLE ( 'NONE', #3377, 6.599999999999998757 ) ;
#12319=CARTESIAN_POINT ( 'NONE',  ( 6.000000000000000000, 0.000000000000000000, 0.000000000000000000 ) ) ;
#12329=ADVANCED_FACE ( 'NONE', ( #4334 ), #1427, .T. ) ;
#12349=DIRECTION ( 'NONE',  ( 0.000000000000000000, 0.000000000000000000, -1.000000000000000000 ) ) ;
#12353=PLANE ( 'NONE',  #9244 ) ;
#12358=CARTESIAN_POINT ( 'NONE',  ( 6.000000000000000000, -2.919948986426538440, -5.057499999999997442 ) ) ;
#12359=VECTOR ( 'NONE', #5988, 1000.000000000000114 ) ;
#12369=EDGE_CURVE ( 'NONE', #11432, #2307, #5356, .T. ) ;
#12459=DIRECTION ( 'NONE',  ( 1.000000000000000000, 0.000000000000000000, 0.000000000000000000 ) ) ;
#12461=( LENGTH_UNIT ( ) NAMED_UNIT ( * ) SI_UNIT ( .MILLI., .METRE. ) );
#12486=AXIS2_PLACEMENT_3D ( 'NONE', #7081, #7021, #9758 ) ;
#12491=SHAPE_DEFINITION_REPRESENTATION ( #117, #10815 ) ;
#12505=EDGE_LOOP ( 'NONE', ( #8592, #46, #6949, #8985 ) ) ;
#12528=TOROIDAL_SURFACE ( 'NONE', #989, 8.400000000000000355, 0.5999999999999999778 ) ;
#12585=COLOUR_RGB('Black',0.12,0.14,0.17);
#12586=FILL_AREA_STYLE_COLOUR('',#12585);
#12587=FILL_AREA_STYLE('',(#12586));
#12588=SURFACE_STYLE_FILL_AREA(#12587);
#12589=SURFACE_SIDE_STYLE('',(#12588));
#12590=SURFACE_STYLE_USAGE(.BOTH.,#12589);
#12591=PRESENTATION_STYLE_ASSIGNMENT((#12590));
ENDSEC;
END-ISO-10303-21;
